ISO-10303-21;
HEADER;
/* Generated by software containing ST-Developer
 * from STEP Tools, Inc. (www.steptools.com) 
 */

FILE_DESCRIPTION(
/* description */ (''),
/* implementation_level */ '2;1');

FILE_NAME(
/* name */ 'Spacer.step',
/* time_stamp */ '2026-09-20T21:58:27+06:00',
/* author */ (''),
/* organization */ (''),
/* preprocessor_version */ 'ST-DEVELOPER v20.2',
/* originating_system */ 'Autodesk Translation Framework v15.15.0.0',
/* authorisation */ '');

FILE_SCHEMA (('AUTOMOTIVE_DESIGN { 1 0 10303 214 3 1 1 }'));
ENDSEC;

DATA;
#10=MECHANICAL_DESIGN_GEOMETRIC_PRESENTATION_REPRESENTATION('',(#63),#2238);
#47=SHAPE_REPRESENTATION_RELATIONSHIP('SRR','None',#2274,#55);
#55=ADVANCED_BREP_SHAPE_REPRESENTATION('',(#71),#2234);
#63=STYLED_ITEM('',(#2321),#71);
#71=MANIFOLD_SOLID_BREP('Spacer',#1210);
#79=FACE_BOUND('',#244,.T.);
#80=FACE_BOUND('',#248,.T.);
#109=PLANE('',#1416);
#110=PLANE('',#1423);
#170=FACE_OUTER_BOUND('',#243,.T.);
#171=FACE_OUTER_BOUND('',#245,.T.);
#172=FACE_OUTER_BOUND('',#246,.T.);
#173=FACE_OUTER_BOUND('',#247,.T.);
#243=EDGE_LOOP('',(#1028));
#244=EDGE_LOOP('',(#1029));
#245=EDGE_LOOP('',(#1030,#1031,#1032,#1033));
#246=EDGE_LOOP('',(#1034,#1035,#1036,#1037));
#247=EDGE_LOOP('',(#1038));
#248=EDGE_LOOP('',(#1039));
#338=LINE('',#2135,#423);
#339=LINE('',#2140,#424);
#423=VECTOR('',#1762,4.5);
#424=VECTOR('',#1769,2.5);
#501=CIRCLE('',#1417,4.5);
#502=CIRCLE('',#1418,2.5);
#503=CIRCLE('',#1420,4.5);
#504=CIRCLE('',#1422,2.5);
#599=VERTEX_POINT('',#2129);
#600=VERTEX_POINT('',#2131);
#601=VERTEX_POINT('',#2134);
#602=VERTEX_POINT('',#2138);
#746=EDGE_CURVE('',#599,#599,#501,.T.);
#747=EDGE_CURVE('',#600,#600,#502,.T.);
#748=EDGE_CURVE('',#599,#601,#338,.T.);
#749=EDGE_CURVE('',#601,#601,#503,.T.);
#750=EDGE_CURVE('',#602,#602,#504,.T.);
#751=EDGE_CURVE('',#602,#600,#339,.T.);
#1028=ORIENTED_EDGE('',*,*,#746,.T.);
#1029=ORIENTED_EDGE('',*,*,#747,.F.);
#1030=ORIENTED_EDGE('',*,*,#746,.F.);
#1031=ORIENTED_EDGE('',*,*,#748,.T.);
#1032=ORIENTED_EDGE('',*,*,#749,.F.);
#1033=ORIENTED_EDGE('',*,*,#748,.F.);
#1034=ORIENTED_EDGE('',*,*,#750,.F.);
#1035=ORIENTED_EDGE('',*,*,#751,.T.);
#1036=ORIENTED_EDGE('',*,*,#747,.T.);
#1037=ORIENTED_EDGE('',*,*,#751,.F.);
#1038=ORIENTED_EDGE('',*,*,#749,.T.);
#1039=ORIENTED_EDGE('',*,*,#750,.T.);
#1129=CYLINDRICAL_SURFACE('',#1419,4.5);
#1130=CYLINDRICAL_SURFACE('',#1421,2.5);
#1186=ADVANCED_FACE('',(#170,#79),#109,.T.);
#1187=ADVANCED_FACE('',(#171),#1129,.T.);
#1188=ADVANCED_FACE('',(#172),#1130,.F.);
#1189=ADVANCED_FACE('',(#173,#80),#110,.T.);
#1210=CLOSED_SHELL('',(#1186,#1187,#1188,#1189));
#1415=AXIS2_PLACEMENT_3D('',#2127,#1752,#1753);
#1416=AXIS2_PLACEMENT_3D('',#2128,#1754,#1755);
#1417=AXIS2_PLACEMENT_3D('',#2130,#1756,#1757);
#1418=AXIS2_PLACEMENT_3D('',#2132,#1758,#1759);
#1419=AXIS2_PLACEMENT_3D('',#2133,#1760,#1761);
#1420=AXIS2_PLACEMENT_3D('',#2136,#1763,#1764);
#1421=AXIS2_PLACEMENT_3D('',#2137,#1765,#1766);
#1422=AXIS2_PLACEMENT_3D('',#2139,#1767,#1768);
#1423=AXIS2_PLACEMENT_3D('',#2141,#1770,#1771);
#1752=DIRECTION('axis',(0.,0.,1.));
#1753=DIRECTION('refdir',(1.,0.,0.));
#1754=DIRECTION('center_axis',(0.,-1.,0.));
#1755=DIRECTION('ref_axis',(1.,0.,0.));
#1756=DIRECTION('center_axis',(0.,-1.,0.));
#1757=DIRECTION('ref_axis',(1.,0.,0.));
#1758=DIRECTION('center_axis',(0.,-1.,0.));
#1759=DIRECTION('ref_axis',(1.,0.,0.));
#1760=DIRECTION('center_axis',(0.,-1.,0.));
#1761=DIRECTION('ref_axis',(1.,0.,0.));
#1762=DIRECTION('',(0.,1.,0.));
#1763=DIRECTION('center_axis',(0.,1.,0.));
#1764=DIRECTION('ref_axis',(1.,0.,0.));
#1765=DIRECTION('center_axis',(0.,-1.,0.));
#1766=DIRECTION('ref_axis',(1.,0.,0.));
#1767=DIRECTION('center_axis',(0.,-1.,0.));
#1768=DIRECTION('ref_axis',(1.,0.,0.));
#1769=DIRECTION('',(0.,-1.,0.));
#1770=DIRECTION('center_axis',(0.,1.,0.));
#1771=DIRECTION('ref_axis',(0.,0.,1.));
#2127=CARTESIAN_POINT('',(0.,0.,0.));
#2128=CARTESIAN_POINT('Origin',(0.,0.,64.2867316297599));
#2129=CARTESIAN_POINT('',(-4.5,0.,64.2867316297599));
#2130=CARTESIAN_POINT('Origin',(0.,0.,64.2867316297599));
#2131=CARTESIAN_POINT('',(-2.5,0.,64.2867316297599));
#2132=CARTESIAN_POINT('Origin',(0.,0.,64.2867316297599));
#2133=CARTESIAN_POINT('Origin',(0.,3.,64.2867316297599));
#2134=CARTESIAN_POINT('',(-4.5,3.,64.2867316297599));
#2135=CARTESIAN_POINT('',(-4.5,3.,64.2867316297599));
#2136=CARTESIAN_POINT('Origin',(0.,3.,64.2867316297599));
#2137=CARTESIAN_POINT('Origin',(0.,3.,64.2867316297599));
#2138=CARTESIAN_POINT('',(-2.5,3.,64.2867316297599));
#2139=CARTESIAN_POINT('Origin',(0.,3.,64.2867316297599));
#2140=CARTESIAN_POINT('',(-2.5,3.,64.2867316297599));
#2141=CARTESIAN_POINT('Origin',(0.,3.,50.));
#2224=UNCERTAINTY_MEASURE_WITH_UNIT(LENGTH_MEASURE(0.01),#2239,
'DISTANCE_ACCURACY_VALUE',
'Maximum model space distance between geometric entities at asserted c
onnectivities');
#2228=UNCERTAINTY_MEASURE_WITH_UNIT(LENGTH_MEASURE(0.01),#2239,
'DISTANCE_ACCURACY_VALUE',
'Maximum model space distance between geometric entities at asserted c
onnectivities');
#2234=(
GEOMETRIC_REPRESENTATION_CONTEXT(3)
GLOBAL_UNCERTAINTY_ASSIGNED_CONTEXT((#2224))
GLOBAL_UNIT_ASSIGNED_CONTEXT((#2239,#2241,#2242))
REPRESENTATION_CONTEXT('','3D')
);
#2238=(
GEOMETRIC_REPRESENTATION_CONTEXT(3)
GLOBAL_UNCERTAINTY_ASSIGNED_CONTEXT((#2228))
GLOBAL_UNIT_ASSIGNED_CONTEXT((#2239,#2241,#2242))
REPRESENTATION_CONTEXT('','3D')
);
#2239=(
LENGTH_UNIT()
NAMED_UNIT(*)
SI_UNIT(.MILLI.,.METRE.)
);
#2241=(
NAMED_UNIT(*)
PLANE_ANGLE_UNIT()
SI_UNIT($,.RADIAN.)
);
#2242=(
NAMED_UNIT(*)
SI_UNIT($,.STERADIAN.)
SOLID_ANGLE_UNIT()
);
#2248=SHAPE_DEFINITION_REPRESENTATION(#2257,#2274);
#2257=PRODUCT_DEFINITION_SHAPE('',$,#2284);
#2274=SHAPE_REPRESENTATION('',(#1415),#2234);
#2278=PRODUCT_DEFINITION_CONTEXT('part definition',#2307,'design');
#2284=PRODUCT_DEFINITION('Spacer','Spacer',#2293,#2278);
#2293=PRODUCT_DEFINITION_FORMATION('',$,#2314);
#2307=APPLICATION_CONTEXT(
'Core Data for Automotive Mechanical Design Process');
#2308=PRODUCT_CONTEXT('part definition',#2307,'mechanical');
#2314=PRODUCT('Spacer','Spacer',$,(#2308));
#2321=PRESENTATION_STYLE_ASSIGNMENT((#2325));
#2325=SURFACE_STYLE_USAGE(.BOTH.,#2329);
#2329=SURFACE_SIDE_STYLE('',(#2333));
#2333=SURFACE_STYLE_FILL_AREA(#2337);
#2337=FILL_AREA_STYLE('Surface - Matte',(#2341));
#2341=FILL_AREA_STYLE_COLOUR('Surface - Matte',#2345);
#2345=COLOUR_RGB('Surface - Matte', 0.31764706, 0.68627451, 0.89019608);
ENDSEC;
END-ISO-10303-21;
